ISO-10303-21;
HEADER;
/* Generated by software containing ST-Developer
 * from STEP Tools, Inc. (www.steptools.com) 
 */

FILE_DESCRIPTION(
/* description */ ('Pipe clamp stand with threaded column'),
/* implementation_level */ '2;1');

FILE_NAME(
/* name */ 'mm liner half (1).step',
/* time_stamp */ '2026-10-27T10:55:48-07:00',
/* author */ (''),
/* organization */ (''),
/* preprocessor_version */ 'ST-DEVELOPER v20.2',
/* originating_system */ 'Autodesk Translation Framework v15.17.0.0',
/* authorisation */ '');

FILE_SCHEMA (('AUTOMOTIVE_DESIGN { 1 0 10303 214 3 1 1 }'));
ENDSEC;

DATA;
#10=MECHANICAL_DESIGN_GEOMETRIC_PRESENTATION_REPRESENTATION('',(#752),#34433);
#704=SHAPE_REPRESENTATION_RELATIONSHIP('SRR','None',#34546,#726);
#726=ADVANCED_BREP_SHAPE_REPRESENTATION('',(#782),#34414);
#752=STYLED_ITEM('',(#34736),#782);
#782=MANIFOLD_SOLID_BREP('Body1',#8779);
#915=PLANE('',#9389);
#916=PLANE('',#9390);
#917=PLANE('',#9391);
#918=PLANE('',#9398);
#1322=FACE_OUTER_BOUND('',#1842,.T.);
#1323=FACE_OUTER_BOUND('',#1843,.T.);
#1324=FACE_OUTER_BOUND('',#1844,.T.);
#1325=FACE_OUTER_BOUND('',#1845,.T.);
#1326=FACE_OUTER_BOUND('',#1846,.T.);
#1327=FACE_OUTER_BOUND('',#1847,.T.);
#1842=EDGE_LOOP('',(#7031,#7032,#7033,#7034));
#1843=EDGE_LOOP('',(#7035,#7036,#7037,#7038));
#1844=EDGE_LOOP('',(#7039,#7040,#7041,#7042));
#1845=EDGE_LOOP('',(#7043,#7044,#7045,#7046));
#1846=EDGE_LOOP('',(#7047,#7048,#7049,#7050));
#1847=EDGE_LOOP('',(#7051,#7052,#7053,#7054));
#2391=LINE('',#28305,#3008);
#2392=LINE('',#28307,#3009);
#2393=LINE('',#28309,#3010);
#2394=LINE('',#28310,#3011);
#2395=LINE('',#28314,#3012);
#2396=LINE('',#28316,#3013);
#2397=LINE('',#28318,#3014);
#2398=LINE('',#28319,#3015);
#3008=VECTOR('',#10734,1.);
#3009=VECTOR('',#10735,1.);
#3010=VECTOR('',#10736,1.);
#3011=VECTOR('',#10737,1.);
#3012=VECTOR('',#10740,1.);
#3013=VECTOR('',#10741,1.);
#3014=VECTOR('',#10742,1.);
#3015=VECTOR('',#10743,1.);
#3370=CIRCLE('',#9392,1.1);
#3371=CIRCLE('',#9393,1.);
#3372=CIRCLE('',#9395,1.);
#3373=CIRCLE('',#9397,1.1);
#3950=VERTEX_POINT('',#28303);
#3951=VERTEX_POINT('',#28304);
#3952=VERTEX_POINT('',#28306);
#3953=VERTEX_POINT('',#28308);
#3954=VERTEX_POINT('',#28312);
#3955=VERTEX_POINT('',#28313);
#3956=VERTEX_POINT('',#28315);
#3957=VERTEX_POINT('',#28317);
#5029=EDGE_CURVE('',#3950,#3951,#2391,.T.);
#5030=EDGE_CURVE('',#3952,#3950,#2392,.T.);
#5031=EDGE_CURVE('',#3953,#3952,#2393,.T.);
#5032=EDGE_CURVE('',#3951,#3953,#2394,.T.);
#5033=EDGE_CURVE('',#3954,#3955,#2395,.T.);
#5034=EDGE_CURVE('',#3956,#3954,#2396,.T.);
#5035=EDGE_CURVE('',#3957,#3956,#2397,.T.);
#5036=EDGE_CURVE('',#3955,#3957,#2398,.T.);
#5037=EDGE_CURVE('',#3951,#3954,#3370,.T.);
#5038=EDGE_CURVE('',#3956,#3953,#3371,.T.);
#5039=EDGE_CURVE('',#3957,#3952,#3372,.T.);
#5040=EDGE_CURVE('',#3950,#3955,#3373,.T.);
#7031=ORIENTED_EDGE('',*,*,#5029,.F.);
#7032=ORIENTED_EDGE('',*,*,#5030,.F.);
#7033=ORIENTED_EDGE('',*,*,#5031,.F.);
#7034=ORIENTED_EDGE('',*,*,#5032,.F.);
#7035=ORIENTED_EDGE('',*,*,#5033,.F.);
#7036=ORIENTED_EDGE('',*,*,#5034,.F.);
#7037=ORIENTED_EDGE('',*,*,#5035,.F.);
#7038=ORIENTED_EDGE('',*,*,#5036,.F.);
#7039=ORIENTED_EDGE('',*,*,#5034,.T.);
#7040=ORIENTED_EDGE('',*,*,#5037,.F.);
#7041=ORIENTED_EDGE('',*,*,#5032,.T.);
#7042=ORIENTED_EDGE('',*,*,#5038,.F.);
#7043=ORIENTED_EDGE('',*,*,#5035,.T.);
#7044=ORIENTED_EDGE('',*,*,#5038,.T.);
#7045=ORIENTED_EDGE('',*,*,#5031,.T.);
#7046=ORIENTED_EDGE('',*,*,#5039,.F.);
#7047=ORIENTED_EDGE('',*,*,#5033,.T.);
#7048=ORIENTED_EDGE('',*,*,#5040,.F.);
#7049=ORIENTED_EDGE('',*,*,#5029,.T.);
#7050=ORIENTED_EDGE('',*,*,#5037,.T.);
#7051=ORIENTED_EDGE('',*,*,#5036,.T.);
#7052=ORIENTED_EDGE('',*,*,#5039,.T.);
#7053=ORIENTED_EDGE('',*,*,#5030,.T.);
#7054=ORIENTED_EDGE('',*,*,#5040,.T.);
#8217=CYLINDRICAL_SURFACE('',#9394,1.);
#8218=CYLINDRICAL_SURFACE('',#9396,1.1);
#8559=ADVANCED_FACE('',(#1322),#915,.F.);
#8560=ADVANCED_FACE('',(#1323),#916,.F.);
#8561=ADVANCED_FACE('',(#1324),#917,.F.);
#8562=ADVANCED_FACE('',(#1325),#8217,.F.);
#8563=ADVANCED_FACE('',(#1326),#8218,.T.);
#8564=ADVANCED_FACE('',(#1327),#918,.T.);
#8779=CLOSED_SHELL('',(#8559,#8560,#8561,#8562,#8563,#8564));
#9388=AXIS2_PLACEMENT_3D('',#28301,#10730,#10731);
#9389=AXIS2_PLACEMENT_3D('',#28302,#10732,#10733);
#9390=AXIS2_PLACEMENT_3D('',#28311,#10738,#10739);
#9391=AXIS2_PLACEMENT_3D('',#28320,#10744,#10745);
#9392=AXIS2_PLACEMENT_3D('',#28321,#10746,#10747);
#9393=AXIS2_PLACEMENT_3D('',#28322,#10748,#10749);
#9394=AXIS2_PLACEMENT_3D('',#28323,#10750,#10751);
#9395=AXIS2_PLACEMENT_3D('',#28324,#10752,#10753);
#9396=AXIS2_PLACEMENT_3D('',#28325,#10754,#10755);
#9397=AXIS2_PLACEMENT_3D('',#28326,#10756,#10757);
#9398=AXIS2_PLACEMENT_3D('',#28327,#10758,#10759);
#10730=DIRECTION('axis',(0.,0.,1.));
#10731=DIRECTION('refdir',(1.,0.,0.));
#10732=DIRECTION('center_axis',(0.,0.,1.));
#10733=DIRECTION('ref_axis',(1.,0.,0.));
#10734=DIRECTION('',(0.,-1.,0.));
#10735=DIRECTION('',(-1.,0.,0.));
#10736=DIRECTION('',(0.,1.,0.));
#10737=DIRECTION('',(1.,0.,0.));
#10738=DIRECTION('center_axis',(0.,0.,1.));
#10739=DIRECTION('ref_axis',(1.,0.,0.));
#10740=DIRECTION('',(0.,1.,0.));
#10741=DIRECTION('',(1.,0.,0.));
#10742=DIRECTION('',(0.,-1.,0.));
#10743=DIRECTION('',(-1.,0.,0.));
#10744=DIRECTION('center_axis',(0.,1.,0.));
#10745=DIRECTION('ref_axis',(1.,0.,0.));
#10746=DIRECTION('center_axis',(0.,1.,0.));
#10747=DIRECTION('ref_axis',(1.,0.,0.));
#10748=DIRECTION('center_axis',(0.,-1.,0.));
#10749=DIRECTION('ref_axis',(1.,0.,0.));
#10750=DIRECTION('center_axis',(0.,1.,0.));
#10751=DIRECTION('ref_axis',(1.,0.,0.));
#10752=DIRECTION('center_axis',(0.,-1.,0.));
#10753=DIRECTION('ref_axis',(1.,0.,0.));
#10754=DIRECTION('center_axis',(0.,1.,0.));
#10755=DIRECTION('ref_axis',(1.,0.,0.));
#10756=DIRECTION('center_axis',(0.,1.,0.));
#10757=DIRECTION('ref_axis',(1.,0.,0.));
#10758=DIRECTION('center_axis',(0.,1.,0.));
#10759=DIRECTION('ref_axis',(1.,0.,0.));
#28301=CARTESIAN_POINT('',(0.,0.,0.));
#28302=CARTESIAN_POINT('Origin',(-4.,-1.1,18.025));
#28303=CARTESIAN_POINT('',(-1.09971587239614,1.,18.025));
#28304=CARTESIAN_POINT('',(-1.09971587239614,-1.,18.025));
#28305=CARTESIAN_POINT('',(-1.09971587239614,-1.,18.025));
#28306=CARTESIAN_POINT('',(-0.99968745115661,1.,18.025));
#28307=CARTESIAN_POINT('',(-2.,1.,18.025));
#28308=CARTESIAN_POINT('',(-0.99968745115661,-1.,18.025));
#28309=CARTESIAN_POINT('',(-0.99968745115661,-1.,18.025));
#28310=CARTESIAN_POINT('',(-2.,-1.,18.025));
#28311=CARTESIAN_POINT('Origin',(-4.,-1.1,18.025));
#28312=CARTESIAN_POINT('',(1.09971587239614,-1.,18.025));
#28313=CARTESIAN_POINT('',(1.09971587239614,1.,18.025));
#28314=CARTESIAN_POINT('',(1.09971587239614,-1.,18.025));
#28315=CARTESIAN_POINT('',(0.99968745115661,-1.,18.025));
#28316=CARTESIAN_POINT('',(-2.,-1.,18.025));
#28317=CARTESIAN_POINT('',(0.99968745115661,1.,18.025));
#28318=CARTESIAN_POINT('',(0.99968745115661,-1.,18.025));
#28319=CARTESIAN_POINT('',(-2.,1.,18.025));
#28320=CARTESIAN_POINT('Origin',(0.,-1.,18.));
#28321=CARTESIAN_POINT('Origin',(0.,-1.,18.));
#28322=CARTESIAN_POINT('Origin',(0.,-1.,18.));
#28323=CARTESIAN_POINT('Origin',(0.,-1.,18.));
#28324=CARTESIAN_POINT('Origin',(0.,1.,18.));
#28325=CARTESIAN_POINT('Origin',(0.,-1.,18.));
#28326=CARTESIAN_POINT('Origin',(0.,1.,18.));
#28327=CARTESIAN_POINT('Origin',(0.,1.,18.));
#34385=UNCERTAINTY_MEASURE_WITH_UNIT(LENGTH_MEASURE(0.001),#34434,
'DISTANCE_ACCURACY_VALUE',
'Maximum model space distance between geometric entities at asserted c
onnectivities');
#34404=UNCERTAINTY_MEASURE_WITH_UNIT(LENGTH_MEASURE(0.001),#34434,
'DISTANCE_ACCURACY_VALUE',
'Maximum model space distance between geometric entities at asserted c
onnectivities');
#34414=(
GEOMETRIC_REPRESENTATION_CONTEXT(3)
GLOBAL_UNCERTAINTY_ASSIGNED_CONTEXT((#34385))
GLOBAL_UNIT_ASSIGNED_CONTEXT((#34434,#34436,#34437))
REPRESENTATION_CONTEXT('','3D')
);
#34433=(
GEOMETRIC_REPRESENTATION_CONTEXT(3)
GLOBAL_UNCERTAINTY_ASSIGNED_CONTEXT((#34404))
GLOBAL_UNIT_ASSIGNED_CONTEXT((#34434,#34436,#34437))
REPRESENTATION_CONTEXT('','3D')
);
#34434=(
LENGTH_UNIT()
NAMED_UNIT(*)
SI_UNIT(.CENTI.,.METRE.)
);
#34436=(
NAMED_UNIT(*)
PLANE_ANGLE_UNIT()
SI_UNIT($,.RADIAN.)
);
#34437=(
NAMED_UNIT(*)
SI_UNIT($,.STERADIAN.)
SOLID_ANGLE_UNIT()
);
#34447=SHAPE_DEFINITION_REPRESENTATION(#34475,#34546);
#34475=PRODUCT_DEFINITION_SHAPE('',$,#34575);
#34546=SHAPE_REPRESENTATION('',(#9388),#34414);
#34565=PRODUCT_DEFINITION_CONTEXT('part definition',#34651,'design');
#34575=PRODUCT_DEFINITION('mm liner half (1)','mm liner half (1)',#34603,
#34565);
#34603=PRODUCT_DEFINITION_FORMATION('',$,#34662);
#34651=APPLICATION_CONTEXT(
'Core Data for Automotive Mechanical Design Process');
#34652=PRODUCT_CONTEXT('part definition',#34651,'mechanical');
#34662=PRODUCT('mm liner half (1)','mm liner half (1)','mm liner half (1)',(#34652));
#34730=COLOUR_RGB('Sky Blue',0.24,0.69,0.87);
#34731=FILL_AREA_STYLE_COLOUR('',#34730);
#34732=FILL_AREA_STYLE('',(#34731));
#34733=SURFACE_STYLE_FILL_AREA(#34732);
#34734=SURFACE_SIDE_STYLE('',(#34733));
#34735=SURFACE_STYLE_USAGE(.BOTH.,#34734);
#34736=PRESENTATION_STYLE_ASSIGNMENT((#34735));
ENDSEC;
END-ISO-10303-21;
